ISO-10303-21;
HEADER;
/* Generated by software containing ST-Developer
 * from STEP Tools, Inc. (www.steptools.com) 
 */

FILE_DESCRIPTION(
/* description */ ('Bin tilter linkage'),
/* implementation_level */ '2;1');

FILE_NAME(
/* name */ 'M4 short cap screw (30).step',
/* time_stamp */ '2026-10-28T03:26:24-07:00',
/* author */ (''),
/* organization */ (''),
/* preprocessor_version */ 'ST-DEVELOPER v20.2',
/* originating_system */ 'Autodesk Translation Framework v15.17.0.0',
/* authorisation */ '');

FILE_SCHEMA (('AUTOMOTIVE_DESIGN { 1 0 10303 214 3 1 1 }'));
ENDSEC;

DATA;
#10=MECHANICAL_DESIGN_GEOMETRIC_PRESENTATION_REPRESENTATION('',(#932),#23728);
#720=SHAPE_REPRESENTATION_RELATIONSHIP('SRR','None',#24186,#826);
#826=ADVANCED_BREP_SHAPE_REPRESENTATION('',(#1045),#23686);
#932=STYLED_ITEM('',(#24772),#1045);
#1045=MANIFOLD_SOLID_BREP('Body1',#12463);
#1384=FACE_BOUND('',#3460,.T.);
#1731=PLANE('',#14754);
#1732=PLANE('',#14759);
#1733=PLANE('',#14762);
#2385=FACE_OUTER_BOUND('',#3459,.T.);
#2386=FACE_OUTER_BOUND('',#3461,.T.);
#2387=FACE_OUTER_BOUND('',#3462,.T.);
#2388=FACE_OUTER_BOUND('',#3463,.T.);
#2389=FACE_OUTER_BOUND('',#3464,.T.);
#3459=EDGE_LOOP('',(#10189));
#3460=EDGE_LOOP('',(#10190));
#3461=EDGE_LOOP('',(#10191,#10192,#10193,#10194));
#3462=EDGE_LOOP('',(#10195));
#3463=EDGE_LOOP('',(#10196,#10197,#10198,#10199));
#3464=EDGE_LOOP('',(#10200));
#4249=LINE('',#21835,#4924);
#4250=LINE('',#21839,#4925);
#4924=VECTOR('',#18040,0.350000000000001);
#4925=VECTOR('',#18045,0.199999999999999);
#5707=CIRCLE('',#14755,0.350000000000001);
#5708=CIRCLE('',#14756,0.199999999999999);
#5709=CIRCLE('',#14758,0.350000000000001);
#5710=CIRCLE('',#14761,0.199999999999999);
#6561=VERTEX_POINT('',#21828);
#6562=VERTEX_POINT('',#21830);
#6563=VERTEX_POINT('',#21833);
#6564=VERTEX_POINT('',#21838);
#7834=EDGE_CURVE('',#6561,#6561,#5707,.T.);
#7835=EDGE_CURVE('',#6562,#6562,#5708,.T.);
#7836=EDGE_CURVE('',#6563,#6563,#5709,.T.);
#7837=EDGE_CURVE('',#6563,#6561,#4249,.T.);
#7838=EDGE_CURVE('',#6562,#6564,#4250,.T.);
#7839=EDGE_CURVE('',#6564,#6564,#5710,.T.);
#10189=ORIENTED_EDGE('',*,*,#7834,.F.);
#10190=ORIENTED_EDGE('',*,*,#7835,.T.);
#10191=ORIENTED_EDGE('',*,*,#7836,.F.);
#10192=ORIENTED_EDGE('',*,*,#7837,.T.);
#10193=ORIENTED_EDGE('',*,*,#7834,.T.);
#10194=ORIENTED_EDGE('',*,*,#7837,.F.);
#10195=ORIENTED_EDGE('',*,*,#7836,.T.);
#10196=ORIENTED_EDGE('',*,*,#7835,.F.);
#10197=ORIENTED_EDGE('',*,*,#7838,.T.);
#10198=ORIENTED_EDGE('',*,*,#7839,.T.);
#10199=ORIENTED_EDGE('',*,*,#7838,.F.);
#10200=ORIENTED_EDGE('',*,*,#7839,.F.);
#11519=CYLINDRICAL_SURFACE('',#14757,0.350000000000001);
#11520=CYLINDRICAL_SURFACE('',#14760,0.199999999999999);
#12110=ADVANCED_FACE('',(#2385,#1384),#1731,.F.);
#12111=ADVANCED_FACE('',(#2386),#11519,.T.);
#12112=ADVANCED_FACE('',(#2387),#1732,.T.);
#12113=ADVANCED_FACE('',(#2388),#11520,.T.);
#12114=ADVANCED_FACE('',(#2389),#1733,.F.);
#12463=CLOSED_SHELL('',(#12110,#12111,#12112,#12113,#12114));
#14753=AXIS2_PLACEMENT_3D('',#21826,#18028,#18029);
#14754=AXIS2_PLACEMENT_3D('',#21827,#18030,#18031);
#14755=AXIS2_PLACEMENT_3D('',#21829,#18032,#18033);
#14756=AXIS2_PLACEMENT_3D('',#21831,#18034,#18035);
#14757=AXIS2_PLACEMENT_3D('',#21832,#18036,#18037);
#14758=AXIS2_PLACEMENT_3D('',#21834,#18038,#18039);
#14759=AXIS2_PLACEMENT_3D('',#21836,#18041,#18042);
#14760=AXIS2_PLACEMENT_3D('',#21837,#18043,#18044);
#14761=AXIS2_PLACEMENT_3D('',#21840,#18046,#18047);
#14762=AXIS2_PLACEMENT_3D('',#21841,#18048,#18049);
#18028=DIRECTION('axis',(0.,0.,1.));
#18029=DIRECTION('refdir',(1.,0.,0.));
#18030=DIRECTION('center_axis',(0.,1.,0.));
#18031=DIRECTION('ref_axis',(1.,0.,0.));
#18032=DIRECTION('center_axis',(0.,1.,0.));
#18033=DIRECTION('ref_axis',(1.,0.,0.));
#18034=DIRECTION('center_axis',(0.,1.,0.));
#18035=DIRECTION('ref_axis',(1.,0.,0.));
#18036=DIRECTION('center_axis',(0.,1.,0.));
#18037=DIRECTION('ref_axis',(1.,0.,0.));
#18038=DIRECTION('center_axis',(0.,1.,0.));
#18039=DIRECTION('ref_axis',(1.,0.,0.));
#18040=DIRECTION('',(0.,-1.,0.));
#18041=DIRECTION('center_axis',(0.,1.,0.));
#18042=DIRECTION('ref_axis',(1.,0.,0.));
#18043=DIRECTION('center_axis',(0.,1.,0.));
#18044=DIRECTION('ref_axis',(1.,0.,0.));
#18045=DIRECTION('',(0.,-1.,0.));
#18046=DIRECTION('center_axis',(0.,1.,0.));
#18047=DIRECTION('ref_axis',(1.,0.,0.));
#18048=DIRECTION('center_axis',(0.,1.,0.));
#18049=DIRECTION('ref_axis',(1.,0.,0.));
#21826=CARTESIAN_POINT('',(0.,0.,0.));
#21827=CARTESIAN_POINT('Origin',(22.893930933827,0.8,27.3496056572921));
#21828=CARTESIAN_POINT('',(22.543930933827,0.8,27.3496056572921));
#21829=CARTESIAN_POINT('Origin',(22.893930933827,0.8,27.3496056572921));
#21830=CARTESIAN_POINT('',(22.693930933827,0.8,27.3496056572921));
#21831=CARTESIAN_POINT('Origin',(22.893930933827,0.8,27.3496056572921));
#21832=CARTESIAN_POINT('Origin',(22.893930933827,0.8,27.3496056572921));
#21833=CARTESIAN_POINT('',(22.543930933827,1.2,27.3496056572921));
#21834=CARTESIAN_POINT('Origin',(22.893930933827,1.2,27.3496056572921));
#21835=CARTESIAN_POINT('',(22.543930933827,0.8,27.3496056572921));
#21836=CARTESIAN_POINT('Origin',(22.893930933827,1.2,27.3496056572921));
#21837=CARTESIAN_POINT('Origin',(22.893930933827,0.1,27.3496056572921));
#21838=CARTESIAN_POINT('',(22.693930933827,0.1,27.3496056572921));
#21839=CARTESIAN_POINT('',(22.693930933827,0.1,27.3496056572921));
#21840=CARTESIAN_POINT('Origin',(22.893930933827,0.1,27.3496056572921));
#21841=CARTESIAN_POINT('Origin',(22.893930933827,0.1,27.3496056572921));
#23569=UNCERTAINTY_MEASURE_WITH_UNIT(LENGTH_MEASURE(0.001),#23729,
'DISTANCE_ACCURACY_VALUE',
'Maximum model space distance between geometric entities at asserted c
onnectivities');
#23611=UNCERTAINTY_MEASURE_WITH_UNIT(LENGTH_MEASURE(0.001),#23729,
'DISTANCE_ACCURACY_VALUE',
'Maximum model space distance between geometric entities at asserted c
onnectivities');
#23686=(
GEOMETRIC_REPRESENTATION_CONTEXT(3)
GLOBAL_UNCERTAINTY_ASSIGNED_CONTEXT((#23569))
GLOBAL_UNIT_ASSIGNED_CONTEXT((#23729,#23731,#23732))
REPRESENTATION_CONTEXT('','3D')
);
#23728=(
GEOMETRIC_REPRESENTATION_CONTEXT(3)
GLOBAL_UNCERTAINTY_ASSIGNED_CONTEXT((#23611))
GLOBAL_UNIT_ASSIGNED_CONTEXT((#23729,#23731,#23732))
REPRESENTATION_CONTEXT('','3D')
);
#23729=(
LENGTH_UNIT()
NAMED_UNIT(*)
SI_UNIT(.CENTI.,.METRE.)
);
#23731=(
NAMED_UNIT(*)
PLANE_ANGLE_UNIT()
SI_UNIT($,.RADIAN.)
);
#23732=(
NAMED_UNIT(*)
SI_UNIT($,.STERADIAN.)
SOLID_ANGLE_UNIT()
);
#23807=SHAPE_DEFINITION_REPRESENTATION(#23923,#24186);
#23923=PRODUCT_DEFINITION_SHAPE('',$,#24303);
#24186=SHAPE_REPRESENTATION('',(#14753),#23686);
#24228=PRODUCT_DEFINITION_CONTEXT('part definition',#24578,'design');
#24303=PRODUCT_DEFINITION('M4 short cap screw (30)',
'M4 short cap screw (30)',#24419,#24228);
#24419=PRODUCT_DEFINITION_FORMATION('',$,#24654);
#24578=APPLICATION_CONTEXT(
'Core Data for Automotive Mechanical Design Process');
#24579=PRODUCT_CONTEXT('part definition',#24578,'mechanical');
#24654=PRODUCT('M4 short cap screw (30)','M4 short cap screw (30)',
'M4 short cap screw (30)',(#24579));
#24766=COLOUR_RGB('Black',0.12,0.14,0.17);
#24767=FILL_AREA_STYLE_COLOUR('',#24766);
#24768=FILL_AREA_STYLE('',(#24767));
#24769=SURFACE_STYLE_FILL_AREA(#24768);
#24770=SURFACE_SIDE_STYLE('',(#24769));
#24771=SURFACE_STYLE_USAGE(.BOTH.,#24770);
#24772=PRESENTATION_STYLE_ASSIGNMENT((#24771));
ENDSEC;
END-ISO-10303-21;
